ISO-10303-21;
HEADER;
FILE_DESCRIPTION((''),'2;1');
FILE_NAME('Spring_Washer_1.step','2026-10-09T11:34:15-07:00',(''),(''),'','','');
FILE_SCHEMA (('AUTOMOTIVE_DESIGN { 1 0 10303 214 3 1 1 }'));
ENDSEC;
DATA;
#10=MECHANICAL_DESIGN_GEOMETRIC_PRESENTATION_REPRESENTATION('',(#634),#117170);
#592=SHAPE_REPRESENTATION_RELATIONSHIP('SRR','None',#117247,#613) ;
#613=ADVANCED_BREP_SHAPE_REPRESENTATION('',(#655),#117155) ;
#634=STYLED_ITEM('',(#117355),#655) ;
#655=MANIFOLD_SOLID_BREP('Body1',#49063) ;
#729=FACE_BOUND('',#15258,.T.) ;
#2482=PLANE('',#51992) ;
#4265=LINE('',#87485,#7479) ;
#4266=LINE('',#87490,#7480) ;
#7479=VECTOR('',#61688,2.) ;
#7480=VECTOR('',#61695,2.4) ;
#9987=CYLINDRICAL_SURFACE('',#51988,2.) ;
#9988=CYLINDRICAL_SURFACE('',#51990,2.4) ;
#12103=FACE_OUTER_BOUND('',#15254,.T.) ;
#12104=FACE_OUTER_BOUND('',#15255,.T.) ;
#12105=FACE_OUTER_BOUND('',#15256,.T.) ;
#12106=FACE_OUTER_BOUND('',#15257,.T.) ;
#15254=EDGE_LOOP('',(#37274,#37275,#37276,#37277,#37278,#37279)) ;
#15255=EDGE_LOOP('',(#37280,#37281,#37282,#37283,#37284)) ;
#15256=EDGE_LOOP('',(#37285,#37286,#37287,#37288,#37289)) ;
#15257=EDGE_LOOP('',(#37290)) ;
#15258=EDGE_LOOP('',(#37291)) ;
#18386=CIRCLE('',#51983,2.) ;
#18387=CIRCLE('',#51984,0.45) ;
#18388=CIRCLE('',#51985,2.4) ;
#18389=CIRCLE('',#51986,2.4) ;
#18390=CIRCLE('',#51987,2.) ;
#18391=CIRCLE('',#51989,2.) ;
#18392=CIRCLE('',#51991,2.4) ;
#21376=VERTEX_POINT('',#87474) ;
#21377=VERTEX_POINT('',#87475) ;
#21378=VERTEX_POINT('',#87477) ;
#21379=VERTEX_POINT('',#87479) ;
#21380=VERTEX_POINT('',#87484) ;
#21381=VERTEX_POINT('',#87488) ;
#26915=EDGE_CURVE('',#21376,#21377,#18386,.T.) ;
#26916=EDGE_CURVE('',#21377,#21378,#18387,.T.) ;
#26917=EDGE_CURVE('',#21379,#21378,#18388,.T.) ;
#26918=EDGE_CURVE('',#21378,#21379,#18389,.T.) ;
#26919=EDGE_CURVE('',#21377,#21376,#18390,.T.) ;
#26920=EDGE_CURVE('',#21376,#21380,#4265,.T.) ;
#26921=EDGE_CURVE('',#21380,#21380,#18391,.T.) ;
#26922=EDGE_CURVE('',#21381,#21381,#18392,.T.) ;
#26923=EDGE_CURVE('',#21381,#21379,#4266,.T.) ;
#37274=ORIENTED_EDGE('',*,*,#26915,.T.) ;
#37275=ORIENTED_EDGE('',*,*,#26916,.T.) ;
#37276=ORIENTED_EDGE('',*,*,#26917,.F.) ;
#37277=ORIENTED_EDGE('',*,*,#26918,.F.) ;
#37278=ORIENTED_EDGE('',*,*,#26916,.F.) ;
#37279=ORIENTED_EDGE('',*,*,#26919,.T.) ;
#37280=ORIENTED_EDGE('',*,*,#26915,.F.) ;
#37281=ORIENTED_EDGE('',*,*,#26920,.T.) ;
#37282=ORIENTED_EDGE('',*,*,#26921,.F.) ;
#37283=ORIENTED_EDGE('',*,*,#26920,.F.) ;
#37284=ORIENTED_EDGE('',*,*,#26919,.F.) ;
#37285=ORIENTED_EDGE('',*,*,#26922,.F.) ;
#37286=ORIENTED_EDGE('',*,*,#26923,.T.) ;
#37287=ORIENTED_EDGE('',*,*,#26917,.T.) ;
#37288=ORIENTED_EDGE('',*,*,#26918,.T.) ;
#37289=ORIENTED_EDGE('',*,*,#26923,.F.) ;
#37290=ORIENTED_EDGE('',*,*,#26922,.T.) ;
#37291=ORIENTED_EDGE('',*,*,#26921,.T.) ;
#45694=TOROIDAL_SURFACE('',#51982,2.45,0.45) ;
#47321=ADVANCED_FACE('',(#12103),#45694,.T.) ;
#47322=ADVANCED_FACE('',(#12104),#9987,.F.) ;
#47323=ADVANCED_FACE('',(#12105),#9988,.T.) ;
#47324=ADVANCED_FACE('',(#12106,#729),#2482,.T.) ;
#49063=CLOSED_SHELL('',(#47321,#47322,#47323,#47324)) ;
#51981=AXIS2_PLACEMENT_3D('',#87472,#61672,#61673) ;
#51982=AXIS2_PLACEMENT_3D('',#87473,#61674,#61675) ;
#51983=AXIS2_PLACEMENT_3D('',#87476,#61676,#61677) ;
#51984=AXIS2_PLACEMENT_3D('',#87478,#61678,#61679) ;
#51985=AXIS2_PLACEMENT_3D('',#87480,#61680,#61681) ;
#51986=AXIS2_PLACEMENT_3D('',#87481,#61682,#61683) ;
#51987=AXIS2_PLACEMENT_3D('',#87482,#61684,#61685) ;
#51988=AXIS2_PLACEMENT_3D('',#87483,#61686,#61687) ;
#51989=AXIS2_PLACEMENT_3D('',#87486,#61689,#61690) ;
#51990=AXIS2_PLACEMENT_3D('',#87487,#61691,#61692) ;
#51991=AXIS2_PLACEMENT_3D('',#87489,#61693,#61694) ;
#51992=AXIS2_PLACEMENT_3D('',#87491,#61696,#61697) ;
#61672=DIRECTION('axis',(0.,0.,1.)) ;
#61673=DIRECTION('refdir',(1.,0.,0.)) ;
#61674=DIRECTION('center_axis',(0.,-5.60383084497445E-34,1.)) ;
#61675=DIRECTION('ref_axis',(-1.,0.,0.)) ;
#61676=DIRECTION('center_axis',(0.,5.60383084497445E-34,-1.)) ;
#61677=DIRECTION('ref_axis',(-1.,0.,0.)) ;
#61678=DIRECTION('center_axis',(0.,1.,5.60383084497445E-34)) ;
#61679=DIRECTION('ref_axis',(1.,0.,0.)) ;
#61680=DIRECTION('center_axis',(2.52374105052742E-18,5.60383084497445E-34,
-1.)) ;
#61681=DIRECTION('ref_axis',(1.,3.40207761657885E-68,2.52374105052742E-18)) ;
#61682=DIRECTION('center_axis',(2.52374105052742E-18,5.60383084497445E-34,
-1.)) ;
#61683=DIRECTION('ref_axis',(1.,3.40207761657885E-68,2.52374105052742E-18)) ;
#61684=DIRECTION('center_axis',(0.,5.60383084497445E-34,-1.)) ;
#61685=DIRECTION('ref_axis',(-1.,0.,0.)) ;
#61686=DIRECTION('center_axis',(0.,0.,-1.)) ;
#61687=DIRECTION('ref_axis',(1.,0.,0.)) ;
#61688=DIRECTION('',(0.,0.,-1.)) ;
#61689=DIRECTION('center_axis',(-2.52374105052742E-18,-5.60383084497445E-34,
1.)) ;
#61690=DIRECTION('ref_axis',(1.,3.40207761657885E-68,2.52374105052742E-18)) ;
#61691=DIRECTION('center_axis',(0.,0.,-1.)) ;
#61692=DIRECTION('ref_axis',(1.,0.,0.)) ;
#61693=DIRECTION('center_axis',(2.52374105052742E-18,5.60383084497445E-34,
-1.)) ;
#61694=DIRECTION('ref_axis',(1.,3.40207761657885E-68,2.52374105052742E-18)) ;
#61695=DIRECTION('',(0.,0.,1.)) ;
#61696=DIRECTION('center_axis',(2.52374105052742E-18,5.60383084497445E-34,
-1.)) ;
#61697=DIRECTION('ref_axis',(1.,3.40207761657885E-68,2.52374105052742E-18)) ;
#87472=CARTESIAN_POINT('',(0.,0.,0.)) ;
#87473=CARTESIAN_POINT('Origin',(64.1568347953872,220.146231446812,30.2741067480597)) ;
#87474=CARTESIAN_POINT('',(62.1568347953872,220.146231446812,30.2741067480597)) ;
#87475=CARTESIAN_POINT('',(66.1568347953872,220.146231446812,30.2741067480597)) ;
#87476=CARTESIAN_POINT('Origin',(64.1568347953872,220.146231446812,30.2741067480597)) ;
#87477=CARTESIAN_POINT('',(66.5568347953872,220.146231446812,30.7213203435596)) ;
#87478=CARTESIAN_POINT('Origin',(66.6068347953872,220.146231446812,30.2741067480597)) ;
#87479=CARTESIAN_POINT('',(61.7568347953872,220.146231446812,30.7213203435596)) ;
#87480=CARTESIAN_POINT('Origin',(64.1568347953872,220.146231446812,30.7213203435596)) ;
#87481=CARTESIAN_POINT('Origin',(64.1568347953872,220.146231446812,30.7213203435596)) ;
#87482=CARTESIAN_POINT('Origin',(64.1568347953872,220.146231446812,30.2741067480597)) ;
#87483=CARTESIAN_POINT('Origin',(64.1568347953872,220.146231446812,30.7213203435596)) ;
#87484=CARTESIAN_POINT('',(62.1568347953872,220.146231446812,28.7213203435596)) ;
#87485=CARTESIAN_POINT('',(62.1568347953872,220.146231446812,30.7213203435596)) ;
#87486=CARTESIAN_POINT('Origin',(64.1568347953872,220.146231446812,28.7213203435596)) ;
#87487=CARTESIAN_POINT('Origin',(64.1568347953872,220.146231446812,30.7213203435596)) ;
#87488=CARTESIAN_POINT('',(61.7568347953872,220.146231446812,28.7213203435596)) ;
#87489=CARTESIAN_POINT('Origin',(64.1568347953872,220.146231446812,28.7213203435596)) ;
#87490=CARTESIAN_POINT('',(61.7568347953872,220.146231446812,30.7213203435596)) ;
#87491=CARTESIAN_POINT('Origin',(64.1568347953872,220.146231446812,28.7213203435596)) ;
#117132=UNCERTAINTY_MEASURE_WITH_UNIT(LENGTH_MEASURE(0.01),#117171,
'DISTANCE_ACCURACY_VALUE',
'Maximum model space distance between geometric entities at asserted c
onnectivities') ;
#117147=UNCERTAINTY_MEASURE_WITH_UNIT(LENGTH_MEASURE(0.01),#117171,
'DISTANCE_ACCURACY_VALUE',
'Maximum model space distance between geometric entities at asserted c
onnectivities') ;
#117155=(
GEOMETRIC_REPRESENTATION_CONTEXT(3)
GLOBAL_UNCERTAINTY_ASSIGNED_CONTEXT((#117132))
GLOBAL_UNIT_ASSIGNED_CONTEXT((#117171,#117173,#117174))
REPRESENTATION_CONTEXT('','3D')
) ;
#117170=(
GEOMETRIC_REPRESENTATION_CONTEXT(3)
GLOBAL_UNCERTAINTY_ASSIGNED_CONTEXT((#117147))
GLOBAL_UNIT_ASSIGNED_CONTEXT((#117171,#117173,#117174))
REPRESENTATION_CONTEXT('','3D')
) ;
#117171=(
LENGTH_UNIT()
NAMED_UNIT(*)
SI_UNIT(.MILLI.,.METRE.)
) ;
#117173=(
NAMED_UNIT(*)
PLANE_ANGLE_UNIT()
SI_UNIT($,.RADIAN.)
) ;
#117174=(
NAMED_UNIT(*)
SI_UNIT($,.STERADIAN.)
SOLID_ANGLE_UNIT()
) ;
#117182=SHAPE_DEFINITION_REPRESENTATION(#117204,#117247) ;
#117204=PRODUCT_DEFINITION_SHAPE('',$,#117270) ;
#117247=SHAPE_REPRESENTATION('',(#51981),#117155) ;
#117262=PRODUCT_DEFINITION_CONTEXT('part definition',#117330,'design') ;
#117270=PRODUCT_DEFINITION('Spring_Washer_1','Spring_Washer_1',#117292,
#117262) ;
#117292=PRODUCT_DEFINITION_FORMATION('',$,#117339) ;
#117330=APPLICATION_CONTEXT(
'Core Data for Automotive Mechanical Design Process') ;
#117331=PRODUCT_CONTEXT('part definition',#117330,'mechanical') ;
#117339=PRODUCT('Spring_Washer_1','Spring_Washer_1',$,(#117331)) ;
#117355=PRESENTATION_STYLE_ASSIGNMENT((#117357)) ;
#117357=SURFACE_STYLE_USAGE(.BOTH.,#117359) ;
#117359=SURFACE_SIDE_STYLE('',(#117361)) ;
#117361=SURFACE_STYLE_FILL_AREA(#117363) ;
#117363=FILL_AREA_STYLE('Opaque(160,160,160)',(#117365)) ;
#117365=FILL_AREA_STYLE_COLOUR('Opaque(160,160,160)',#117367) ;
#117367=COLOUR_RGB('Opaque(160,160,160)', 0.09019608, 0.27058824, 0.51372549) ;
ENDSEC;
END-ISO-10303-21;
